ISO-10303-21;
HEADER;
FILE_DESCRIPTION (('STEP AP214'),
    '1' );
FILE_NAME ('socket button head screw_iso_ISO 7380 - M5 x 20 - 20N.step',
    '2026-10-08T09:53:37',
    ( '' ),
    ( '' ),
    'SwSTEP 2.0',
    'SolidWorks 2026',
    '' );
FILE_SCHEMA (( 'AUTOMOTIVE_DESIGN' ));
ENDSEC;

DATA;
#100=DIRECTION ( 'NONE',  ( 0.000000000000000000, 0.000000000000000000, 1.000000000000000000 ) ) ;
#223=ORIENTED_EDGE ( 'NONE', *, *, #32015, .F. ) ;
#412=LINE ( 'NONE', #28552, #45572 ) ;
#552=CARTESIAN_POINT ( 'NONE',  ( 0.000000000000000000, -1.732050807568877859, -1.752539433813135784E-17 ) ) ;
#571=FACE_OUTER_BOUND ( 'NONE', #48022, .T. ) ;
#602=( NAMED_UNIT ( * ) PLANE_ANGLE_UNIT ( ) SI_UNIT ( $, .RADIAN. ) );
#1127=AXIS2_PLACEMENT_3D ( 'NONE', #39142, #38401, #33110 ) ;
#1244=VERTEX_POINT ( 'NONE', #49151 ) ;
#1273=LINE ( 'NONE', #62545, #61221 ) ;
#1316=EDGE_CURVE ( 'NONE', #57811, #52268, #8931, .T. ) ;
#1429=CARTESIAN_POINT ( 'NONE',  ( 1.560000000000000053, -0.8660254037844384856, -1.500000000000000000 ) ) ;
#1561=STYLED_ITEM ( 'NONE', ( #5849 ), #37264 ) ;
#1830=DIRECTION ( 'NONE',  ( 0.000000000000000000, 0.000000000000000000, 1.000000000000000000 ) ) ;
#1866=CARTESIAN_POINT ( 'NONE',  ( 2.369999999999999662, 4.749999999999999112, 0.000000000000000000 ) ) ;
#1920=ORIENTED_EDGE ( 'NONE', *, *, #51945, .T. ) ;
#1994=VECTOR ( 'NONE', #52722, 1000.000000000000000 ) ;
#2233=( GEOMETRIC_REPRESENTATION_CONTEXT ( 3 ) GLOBAL_UNCERTAINTY_ASSIGNED_CONTEXT ( ( #8273 ) ) GLOBAL_UNIT_ASSIGNED_CONTEXT ( ( #17270, #61286, #16524 ) ) REPRESENTATION_CONTEXT ( 'NONE', 'WORKASPACE' ) );
#2340=VECTOR ( 'NONE', #20874, 1000.000000000000000 ) ;
#2366=ORIENTED_EDGE ( 'NONE', *, *, #47957, .F. ) ;
#2397=VERTEX_POINT ( 'NONE', #57127 ) ;
#2493=CARTESIAN_POINT ( 'NONE',  ( 2.750000000000000000, 0.000000000000000000, 0.000000000000000000 ) ) ;
#2508=UNCERTAINTY_MEASURE_WITH_UNIT (LENGTH_MEASURE( 1.000000000000000082E-05 ), #45710, 'distance_accuracy_value', 'NONE');
#2572=VERTEX_POINT ( 'NONE', #6721 ) ;
#2590=CARTESIAN_POINT ( 'NONE',  ( 1.560000000000000053, -1.732050807568877859, -1.752539433813135784E-17 ) ) ;
#2692=DIRECTION ( 'NONE',  ( 0.000000000000000000, 0.000000000000000000, 1.000000000000000000 ) ) ;
#2811=DIRECTION ( 'NONE',  ( 0.000000000000000000, 0.000000000000000000, 1.000000000000000000 ) ) ;
#2927=CARTESIAN_POINT ( 'NONE',  ( 1.560000000000000053, 0.8660254037844389297, 1.500000000000000000 ) ) ;
#2947=LINE ( 'NONE', #2590, #8833 ) ;
#3011=ORIENTED_EDGE ( 'NONE', *, *, #64917, .F. ) ;
#3125=DIRECTION ( 'NONE',  ( -1.000000000000000000, -0.000000000000000000, -0.000000000000000000 ) ) ;
#3465=DIRECTION ( 'NONE',  ( 1.000000000000000000, 0.000000000000000000, 0.000000000000000000 ) ) ;
#3698=LINE ( 'NONE', #32605, #43884 ) ;
#3825=ORIENTED_EDGE ( 'NONE', *, *, #61696, .F. ) ;
#3915=DIRECTION ( 'NONE',  ( -1.000000000000000000, -0.000000000000000000, -0.000000000000000000 ) ) ;
#4334=DIRECTION ( 'NONE',  ( -1.000000000000000000, -0.000000000000000000, -0.000000000000000000 ) ) ;
#4525=SURFACE_STYLE_USAGE ( .BOTH. , #56392 ) ;
#4613=DIRECTION ( 'NONE',  ( -1.000000000000000000, -0.000000000000000000, -0.000000000000000000 ) ) ;
#4677=LINE ( 'NONE', #51633, #26259 ) ;
#4691=DIRECTION ( 'NONE',  ( 1.000000000000000000, 0.000000000000000000, 0.000000000000000000 ) ) ;
#4870=DIRECTION ( 'NONE',  ( 0.000000000000000000, 0.8660254037844384856, 0.5000000000000004441 ) ) ;
#4892=LINE ( 'NONE', #49963, #37491 ) ;
#4942=ORIENTED_EDGE ( 'NONE', *, *, #66718, .T. ) ;
#4976=EDGE_CURVE ( 'NONE', #52268, #28753, #8460, .T. ) ;
#5087=ORIENTED_EDGE ( 'NONE', *, *, #25952, .F. ) ;
#5091=DIRECTION ( 'NONE',  ( -1.000000000000000000, -0.000000000000000000, -0.000000000000000000 ) ) ;
#5163=DIRECTION ( 'NONE',  ( 0.000000000000000000, 0.000000000000000000, 1.000000000000000000 ) ) ;
#5571=ORIENTED_EDGE ( 'NONE', *, *, #4976, .F. ) ;
#5593=DIRECTION ( 'NONE',  ( -1.000000000000000000, -0.000000000000000000, -0.000000000000000000 ) ) ;
#5608=DIRECTION ( 'NONE',  ( 0.000000000000000000, 0.000000000000000000, 1.000000000000000000 ) ) ;
#5737=DIRECTION ( 'NONE',  ( -0.7071067811865479058, 8.659560562354930393E-17, -0.7071067811865472397 ) ) ;
#5743=CARTESIAN_POINT ( 'NONE',  ( 2.426025403784448642, 2.655529440325959183E-32, -2.168404344971008868E-16 ) ) ;
#5765=CARTESIAN_POINT ( 'NONE',  ( 1.560000000000000053, 0.000000000000000000, 2.999999999999998668 ) ) ;
#5792=EDGE_CURVE ( 'NONE', #67138, #14148, #11319, .T. ) ;
#5810=EDGE_CURVE ( 'NONE', #12127, #28753, #63220, .T. ) ;
#5849=PRESENTATION_STYLE_ASSIGNMENT (( #35512 ) ) ;
#5975=AXIS2_PLACEMENT_3D ( 'NONE', #43004, #65571, #2811 ) ;
#6045=ORIENTED_EDGE ( 'NONE', *, *, #32015, .T. ) ;
#6047=VECTOR ( 'NONE', #41113, 1000.000000000000114 ) ;
#6101=FACE_OUTER_BOUND ( 'NONE', #65148, .T. ) ;
#6105=VERTEX_POINT ( 'NONE', #39076 ) ;
#6163=ORIENTED_EDGE ( 'NONE', *, *, #71614, .T. ) ;
#6175=FACE_OUTER_BOUND ( 'NONE', #34393, .T. ) ;
#6343=ORIENTED_EDGE ( 'NONE', *, *, #73169, .F. ) ;
#6380=VERTEX_POINT ( 'NONE', #42040 ) ;
#6721=CARTESIAN_POINT ( 'NONE',  ( 2.750000000000000000, 0.000000000000000000, 2.699999999999999734 ) ) ;
#6875=FACE_OUTER_BOUND ( 'NONE', #39427, .T. ) ;
#7010=LINE ( 'NONE', #1429, #47202 ) ;
#7058=ORIENTED_EDGE ( 'NONE', *, *, #58375, .T. ) ;
#7173=LINE ( 'NONE', #54149, #38278 ) ;
#7179=CARTESIAN_POINT ( 'NONE',  ( 2.949999999999999734, 3.061616997868382648E-16, -2.499999999999999556 ) ) ;
#7254=CARTESIAN_POINT ( 'NONE',  ( 22.75000000000000000, 0.000000000000000000, 0.000000000000000000 ) ) ;
#7409=FACE_OUTER_BOUND ( 'NONE', #16121, .T. ) ;
#7461=ADVANCED_FACE ( 'NONE', ( #46545 ), #58191, .T. ) ;
#7486=FACE_OUTER_BOUND ( 'NONE', #35227, .T. ) ;
#7641=EDGE_CURVE ( 'NONE', #14148, #1244, #66436, .T. ) ;
#7971=AXIS2_PLACEMENT_3D ( 'NONE', #58298, #69578, #100 ) ;
#8072=DIRECTION ( 'NONE',  ( 0.000000000000000000, 0.000000000000000000, 1.000000000000000000 ) ) ;
#8273=UNCERTAINTY_MEASURE_WITH_UNIT (LENGTH_MEASURE( 1.000000000000000082E-05 ), #17270, 'distance_accuracy_value', 'NONE');
#8460=LINE ( 'NONE', #60708, #13470 ) ;
#8664=FACE_OUTER_BOUND ( 'NONE', #51946, .T. ) ;
#8668=EDGE_CURVE ( 'NONE', #71835, #6380, #19383, .T. ) ;
#8833=VECTOR ( 'NONE', #14929, 1000.000000000000000 ) ;
#8839=DIRECTION ( 'NONE',  ( 1.000000000000000000, 0.000000000000000000, 0.000000000000000000 ) ) ;
#8871=VECTOR ( 'NONE', #4334, 1000.000000000000000 ) ;
#8931=LINE ( 'NONE', #55162, #57629 ) ;
#9097=EDGE_CURVE ( 'NONE', #67138, #40854, #74302, .T. ) ;
#9146=ORIENTED_EDGE ( 'NONE', *, *, #50430, .F. ) ;
#9180=DIRECTION ( 'NONE',  ( -1.000000000000000000, 0.000000000000000000, 0.000000000000000000 ) ) ;
#9315=CARTESIAN_POINT ( 'NONE',  ( 0.000000000000000000, 2.375000000000000444, 0.000000000000000000 ) ) ;
#9365=CARTESIAN_POINT ( 'NONE',  ( 1.560000000000000053, 0.000000000000000000, 0.000000000000000000 ) ) ;
#9491=CARTESIAN_POINT ( 'NONE',  ( 1.560000000000000053, 1.299038105676658228, 0.7500000000000009992 ) ) ;
#9509=EDGE_LOOP ( 'NONE', ( #29607, #40610 ) ) ;
#9594=CIRCLE ( 'NONE', #51606, 1.500000000000000000 ) ;
#9771=FILL_AREA_STYLE_COLOUR ( '', #45476 ) ;
#9820=DIRECTION ( 'NONE',  ( 0.000000000000000000, 0.000000000000000000, 1.000000000000000000 ) ) ;
#9878=LINE ( 'NONE', #30304, #62399 ) ;
#10271=FACE_OUTER_BOUND ( 'NONE', #61898, .T. ) ;
#10274=CARTESIAN_POINT ( 'NONE',  ( 2.949999999999999734, 0.000000000000000000, 2.499999999999999556 ) ) ;
#10473=PLANE ( 'NONE',  #50361 ) ;
#10504=EDGE_CURVE ( 'NONE', #70995, #59464, #20372, .T. ) ;
#10739=DIRECTION ( 'NONE',  ( 0.000000000000000000, 0.000000000000000000, 1.000000000000000000 ) ) ;
#10787=ADVANCED_FACE ( 'NONE', ( #51070 ), #10473, .T. ) ;
#10803=AXIS2_PLACEMENT_3D ( 'NONE', #21181, #38118, #27948 ) ;
#11139=DIRECTION ( 'NONE',  ( 0.000000000000000000, 0.000000000000000000, 1.000000000000000000 ) ) ;
#11153=CARTESIAN_POINT ( 'NONE',  ( 1.560000000000000053, 0.000000000000000000, 2.999999999999998668 ) ) ;
#11319=LINE ( 'NONE', #69213, #31949 ) ;
#11321=CARTESIAN_POINT ( 'NONE',  ( 22.75000000000000000, 0.000000000000000000, 0.000000000000000000 ) ) ;
#11382=FACE_OUTER_BOUND ( 'NONE', #53895, .T. ) ;
#11422=DIRECTION ( 'NONE',  ( -0.5000000000000042188, 0.000000000000000000, 0.8660254037844361541 ) ) ;
#11509=AXIS2_PLACEMENT_3D ( 'NONE', #68583, #63687, #33983 ) ;
#11643=AXIS2_PLACEMENT_3D ( 'NONE', #34520, #57467, #5608 ) ;
#11827=CARTESIAN_POINT ( 'NONE',  ( 2.426025403784448642, 2.168404344971008868E-16, 0.000000000000000000 ) ) ;
#11832=CIRCLE ( 'NONE', #69491, 4.750000000000000000 ) ;
#11918=ORIENTED_EDGE ( 'NONE', *, *, #61696, .T. ) ;
#11954=EDGE_LOOP ( 'NONE', ( #4942, #64743, #36065, #52696, #7058, #27917 ) ) ;
#12089=DIRECTION ( 'NONE',  ( -1.000000000000000000, 0.000000000000000000, 0.000000000000000000 ) ) ;
#12127=VERTEX_POINT ( 'NONE', #36370 ) ;
#12138=DIRECTION ( 'NONE',  ( -1.000000000000000000, -0.000000000000000000, -0.000000000000000000 ) ) ;
#12173=DIRECTION ( 'NONE',  ( 0.000000000000000000, 0.000000000000000000, 1.000000000000000000 ) ) ;
#12205=SURFACE_SIDE_STYLE ('',( #24246 ) ) ;
#12228=PLANE ( 'NONE',  #17436 ) ;
#12384=ORIENTED_EDGE ( 'NONE', *, *, #9097, .F. ) ;
#12426=DIRECTION ( 'NONE',  ( 0.000000000000000000, 1.224646799147353207E-16, -1.000000000000000000 ) ) ;
#12526=AXIS2_PLACEMENT_3D ( 'NONE', #54334, #31385, #8839 ) ;
#12590=VECTOR ( 'NONE', #61790, 1000.000000000000000 ) ;
#12796=PLANE ( 'NONE',  #59058 ) ;
#12843=ORIENTED_EDGE ( 'NONE', *, *, #27689, .T. ) ;
#13145=VERTEX_POINT ( 'NONE', #32029 ) ;
#13160=EDGE_CURVE ( 'NONE', #53011, #70414, #57227, .T. ) ;
#13176=CIRCLE ( 'NONE', #23983, 1.500000000000000000 ) ;
#13470=VECTOR ( 'NONE', #26101, 1000.000000000000000 ) ;
#13540=CARTESIAN_POINT ( 'NONE',  ( 1.560000000000000053, 1.732050807568878747, 7.017607234860990640E-28 ) ) ;
#13778=ORIENTED_EDGE ( 'NONE', *, *, #15692, .T. ) ;
#14147=EDGE_CURVE ( 'NONE', #2572, #26241, #57231, .T. ) ;
#14148=VERTEX_POINT ( 'NONE', #44767 ) ;
#14192=DIRECTION ( 'NONE',  ( -1.000000000000000000, 0.000000000000000000, -0.000000000000000000 ) ) ;
#14245=ORIENTED_EDGE ( 'NONE', *, *, #43894, .F. ) ;
#14269=DIRECTION ( 'NONE',  ( -0.000000000000000000, -1.000000000000000000, -0.000000000000000000 ) ) ;
#14422=FACE_OUTER_BOUND ( 'NONE', #50569, .T. ) ;
#14460=DIRECTION ( 'NONE',  ( -1.000000000000000000, -0.000000000000000000, -0.000000000000000000 ) ) ;
#14631=DIRECTION ( 'NONE',  ( 0.000000000000000000, 0.000000000000000000, 1.000000000000000000 ) ) ;
#14729=VERTEX_POINT ( 'NONE', #63843 ) ;
#14774=ORIENTED_EDGE ( 'NONE', *, *, #14147, .F. ) ;
#14929=DIRECTION ( 'NONE',  ( -1.000000000000000000, 0.000000000000000000, 0.000000000000000000 ) ) ;
#15391=CARTESIAN_POINT ( 'NONE',  ( 1.560000000000000053, -1.299038105676658450, -0.7500000000000007772 ) ) ;
#15405=VECTOR ( 'NONE', #59414, 1000.000000000000000 ) ;
#15456=FACE_OUTER_BOUND ( 'NONE', #9509, .T. ) ;
#15641=DIRECTION ( 'NONE',  ( -0.000000000000000000, 1.000000000000000000, -0.000000000000000000 ) ) ;
#15663=LINE ( 'NONE', #2927, #31098 ) ;
#15692=EDGE_CURVE ( 'NONE', #46710, #31992, #7010, .T. ) ;
#15817=DIRECTION ( 'NONE',  ( 0.000000000000000000, 0.000000000000000000, -1.000000000000000000 ) ) ;
#16121=EDGE_LOOP ( 'NONE', ( #71449, #47461, #65630, #25143 ) ) ;
#16524=( NAMED_UNIT ( * ) SI_UNIT ( $, .STERADIAN. ) SOLID_ANGLE_UNIT ( ) );
#16548=ORIENTED_EDGE ( 'NONE', *, *, #13160, .T. ) ;
#16846=ORIENTED_EDGE ( 'NONE', *, *, #9097, .T. ) ;
#16863=CARTESIAN_POINT ( 'NONE',  ( 2.369999999999999662, 0.000000000000000000, 0.000000000000000000 ) ) ;
#17001=CARTESIAN_POINT ( 'NONE',  ( 1.560000000000000053, 0.000000000000000000, 2.999999999999998668 ) ) ;
#17161=PLANE ( 'NONE',  #23280 ) ;
#17270=( LENGTH_UNIT ( ) NAMED_UNIT ( * ) SI_UNIT ( .MILLI., .METRE. ) );
#17436=AXIS2_PLACEMENT_3D ( 'NONE', #35530, #35164, #23515 ) ;
#17476=VERTEX_POINT ( 'NONE', #11827 ) ;
#17520=VECTOR ( 'NONE', #72750, 1000.000000000000114 ) ;
#17547=CARTESIAN_POINT ( 'NONE',  ( 0.000000000000000000, -0.8660254037844384856, -1.500000000000000000 ) ) ;
#17705=DIRECTION ( 'NONE',  ( -0.000000000000000000, 0.000000000000000000, 1.000000000000000000 ) ) ;
#17721=AXIS2_PLACEMENT_3D ( 'NONE', #9365, #25920, #38693 ) ;
#18243=FACE_OUTER_BOUND ( 'NONE', #35695, .T. ) ;
#18268=FACE_OUTER_BOUND ( 'NONE', #44837, .T. ) ;
#18402=PRODUCT_DEFINITION_FORMATION_WITH_SPECIFIED_SOURCE ( 'ANY', '', #49365, .NOT_KNOWN. ) ;
#18584=SHAPE_REPRESENTATION_RELATIONSHIP ( 'NONE' , 'NONE' ,  #33525, #37264 ) ;
#18821=ADVANCED_FACE ( 'NONE', ( #18243 ), #12228, .T. ) ;
#18914=CYLINDRICAL_SURFACE ( 'NONE', #53315, 4.750000000000000000 ) ;
#19070=DIRECTION ( 'NONE',  ( -1.000000000000000000, 0.000000000000000000, 0.000000000000000000 ) ) ;
#19245=AXIS2_PLACEMENT_3D ( 'NONE', #17001, #12089, #23738 ) ;
#19259=DIRECTION ( 'NONE',  ( -1.000000000000000000, -0.000000000000000000, -0.000000000000000000 ) ) ;
#19353=AXIS2_PLACEMENT_3D ( 'NONE', #42409, #48413, #14192 ) ;
#19383=CIRCLE ( 'NONE', #24179, 4.750000000000000000 ) ;
#19440=CARTESIAN_POINT ( 'NONE',  ( 1.560000000000000053, 0.000000000000000000, 2.999999999999998668 ) ) ;
#19630=ORIENTED_EDGE ( 'NONE', *, *, #64868, .T. ) ;
#19678=VERTEX_POINT ( 'NONE', #9315 ) ;
#19735=DIRECTION ( 'NONE',  ( 1.000000000000000000, 0.000000000000000000, 0.000000000000000000 ) ) ;
#19806=CARTESIAN_POINT ( 'NONE',  ( 1.560000000000000053, 1.732050807568878747, 7.017607234860990640E-28 ) ) ;
#19813=ORIENTED_EDGE ( 'NONE', *, *, #47957, .T. ) ;
#19913=EDGE_CURVE ( 'NONE', #59706, #48451, #50104, .T. ) ;
#19939=EDGE_LOOP ( 'NONE', ( #37186, #60655, #56872 ) ) ;
#19952=ORIENTED_EDGE ( 'NONE', *, *, #58375, .F. ) ;
#19958=CARTESIAN_POINT ( 'NONE',  ( 2.750000000000000000, 5.817072295949927426E-16, -4.750000000000000000 ) ) ;
#19974=CARTESIAN_POINT ( 'NONE',  ( 1.560000000000000053, -1.732050807568877859, -1.752539433813135784E-17 ) ) ;
#20036=EDGE_LOOP ( 'NONE', ( #32274, #30662, #45050 ) ) ;
#20197=ADVANCED_FACE ( 'NONE', ( #55587 ), #59849, .T. ) ;
#20228=FACE_BOUND ( 'NONE', #11954, .T. ) ;
#20271=ORIENTED_EDGE ( 'NONE', *, *, #46421, .T. ) ;
#20372=CIRCLE ( 'NONE', #28737, 4.750000000000000000 ) ;
#20429=ORIENTED_EDGE ( 'NONE', *, *, #45150, .F. ) ;
#20443=ORIENTED_EDGE ( 'NONE', *, *, #43801, .T. ) ;
#20590=AXIS2_PLACEMENT_3D ( 'NONE', #48578, #19259, #42946 ) ;
#20752=ORIENTED_EDGE ( 'NONE', *, *, #25952, .T. ) ;
#20832=PLANE ( 'NONE',  #31207 ) ;
#20874=DIRECTION ( 'NONE',  ( -1.000000000000000000, 0.000000000000000000, 0.000000000000000000 ) ) ;
#21181=CARTESIAN_POINT ( 'NONE',  ( 2.750000000000000000, 0.000000000000000000, 0.000000000000000000 ) ) ;
#21338=SPHERICAL_SURFACE ( 'NONE', #50994, 5.315148208181397216 ) ;
#21434=ORIENTED_EDGE ( 'NONE', *, *, #51945, .F. ) ;
#21446=ORIENTED_EDGE ( 'NONE', *, *, #64264, .F. ) ;
#21479=FACE_OUTER_BOUND ( 'NONE', #41775, .T. ) ;
#21481=ORIENTED_EDGE ( 'NONE', *, *, #73088, .F. ) ;
#21577=DIRECTION ( 'NONE',  ( 0.000000000000000000, 0.000000000000000000, 1.000000000000000000 ) ) ;
#21605=AXIS2_PLACEMENT_3D ( 'NONE', #72274, #73754, #67006 ) ;
#21630=ORIENTED_EDGE ( 'NONE', *, *, #68496, .F. ) ;
#21789=SURFACE_STYLE_FILL_AREA ( #22171 ) ;
#21921=ORIENTED_EDGE ( 'NONE', *, *, #13160, .F. ) ;
#21953=CARTESIAN_POINT ( 'NONE',  ( 4.755015822784811164, -4.336808689942017736E-16, 0.000000000000000000 ) ) ;
#21976=LINE ( 'NONE', #68219, #8871 ) ;
#22131=DIRECTION ( 'NONE',  ( 0.000000000000000000, -0.5000000000000003331, 0.8660254037844383745 ) ) ;
#22171=FILL_AREA_STYLE ('',( #9771 ) ) ;
#22291=ORIENTED_EDGE ( 'NONE', *, *, #64167, .F. ) ;
#22300=CONICAL_SURFACE ( 'NONE', #31886, 1732.050807568857181, 1.047197551196592746 ) ;
#22356=CONICAL_SURFACE ( 'NONE', #34314, 1732.050807568857181, 1.047197551196592746 ) ;
#22438=ADVANCED_FACE ( 'NONE', ( #68486 ), #12796, .T. ) ;
#22650=ORIENTED_EDGE ( 'NONE', *, *, #8668, .F. ) ;
#22737=AXIS2_PLACEMENT_3D ( 'NONE', #16863, #5593, #56342 ) ;
#22828=ORIENTED_EDGE ( 'NONE', *, *, #58638, .T. ) ;
#22833=EDGE_CURVE ( 'NONE', #70414, #43461, #4892, .T. ) ;
#23165=AXIS2_PLACEMENT_3D ( 'NONE', #29101, #5091, #68608 ) ;
#23280=AXIS2_PLACEMENT_3D ( 'NONE', #11153, #74301, #38612 ) ;
#23434=ADVANCED_FACE ( 'NONE', ( #63712 ), #49531, .F. ) ;
#23473=AXIS2_PLACEMENT_3D ( 'NONE', #53994, #38824, #61764 ) ;
#23515=DIRECTION ( 'NONE',  ( 0.000000000000000000, -0.5000000000000003331, -0.8660254037844383745 ) ) ;
#23630=CARTESIAN_POINT ( 'NONE',  ( 2.369999999999999662, 0.000000000000000000, 0.000000000000000000 ) ) ;
#23706=CARTESIAN_POINT ( 'NONE',  ( 0.000000000000000000, -0.8660254037844384856, 1.500000000000000000 ) ) ;
#23738=DIRECTION ( 'NONE',  ( 0.000000000000000000, 0.000000000000000000, 1.000000000000000000 ) ) ;
#23780=DIRECTION ( 'NONE',  ( -0.000000000000000000, -1.000000000000000000, -0.000000000000000000 ) ) ;
#23831=CARTESIAN_POINT ( 'NONE',  ( 0.000000000000000000, 0.000000000000000000, 0.000000000000000000 ) ) ;
#23843=ORIENTED_EDGE ( 'NONE', *, *, #56543, .T. ) ;
#23851=VERTEX_POINT ( 'NONE', #57883 ) ;
#23953=ORIENTED_EDGE ( 'NONE', *, *, #32730, .F. ) ;
#23983=AXIS2_PLACEMENT_3D ( 'NONE', #38942, #39695, #10739 ) ;
#24132=CARTESIAN_POINT ( 'NONE',  ( 22.75000000000000000, 2.516649172247811061E-16, -2.055000000000000160 ) ) ;
#24179=AXIS2_PLACEMENT_3D ( 'NONE', #23630, #39447, #63868 ) ;
#24193=SPHERICAL_SURFACE ( 'NONE', #11509, 5.315148208181397216 ) ;
#24246=SURFACE_STYLE_FILL_AREA ( #41897 ) ;
#24360=CARTESIAN_POINT ( 'NONE',  ( 0.000000000000000000, 0.8660254037844389297, 1.500000000000000000 ) ) ;
#24457=DIRECTION ( 'NONE',  ( -0.000000000000000000, -0.5000000000000004441, 0.8660254037844383745 ) ) ;
#24605=DIRECTION ( 'NONE',  ( -0.000000000000000000, -0.5000000000000003331, -0.8660254037844384856 ) ) ;
#24728=CARTESIAN_POINT ( 'NONE',  ( 1.560000000000000053, 0.8660254037844389297, -1.500000000000000000 ) ) ;
#24996=VECTOR ( 'NONE', #50469, 999.9999999999998863 ) ;
#25135=ORIENTED_EDGE ( 'NONE', *, *, #1316, .F. ) ;
#25143=ORIENTED_EDGE ( 'NONE', *, *, #26321, .F. ) ;
#25147=DIRECTION ( 'NONE',  ( -0.000000000000000000, 0.000000000000000000, 1.000000000000000000 ) ) ;
#25195=AXIS2_PLACEMENT_3D ( 'NONE', #21953, #12426, #61819 ) ;
#25269=DIRECTION ( 'NONE',  ( 0.000000000000000000, 0.000000000000000000, 1.000000000000000000 ) ) ;
#25324=ADVANCED_FACE ( 'NONE', ( #26248 ), #21338, .T. ) ;
#25464=ADVANCED_FACE ( 'NONE', ( #7409 ), #58530, .T. ) ;
#25595=ORIENTED_EDGE ( 'NONE', *, *, #40910, .T. ) ;
#25723=ORIENTED_EDGE ( 'NONE', *, *, #50731, .T. ) ;
#25920=DIRECTION ( 'NONE',  ( -1.000000000000000000, -0.000000000000000000, -0.000000000000000000 ) ) ;
#25952=EDGE_CURVE ( 'NONE', #59706, #12127, #58084, .T. ) ;
#26101=DIRECTION ( 'NONE',  ( -0.000000000000000000, -1.000000000000000000, -0.000000000000000000 ) ) ;
#26187=DIRECTION ( 'NONE',  ( -0.000000000000000000, 0.5000000000000004441, 0.8660254037844383745 ) ) ;
#26193=CIRCLE ( 'NONE', #72980, 2.500000000000000444 ) ;
#26241=VERTEX_POINT ( 'NONE', #10274 ) ;
#26248=FACE_OUTER_BOUND ( 'NONE', #32902, .T. ) ;
#26259=VECTOR ( 'NONE', #39249, 1000.000000000000114 ) ;
#26321=EDGE_CURVE ( 'NONE', #2397, #26241, #68163, .T. ) ;
#26454=DIRECTION ( 'NONE',  ( 0.000000000000000000, -1.224646799147353207E-16, 1.000000000000000000 ) ) ;
#26474=ADVANCED_FACE ( 'NONE', ( #11382 ), #34316, .T. ) ;
#26500=ADVANCED_FACE ( 'NONE', ( #71474 ), #59852, .T. ) ;
#26506=DIRECTION ( 'NONE',  ( -1.000000000000000000, -0.000000000000000000, -0.000000000000000000 ) ) ;
#26562=PRODUCT_DEFINITION_SHAPE ( 'NONE', 'NONE',  #30197 ) ;
#26602=VERTEX_POINT ( 'NONE', #69153 ) ;
#26732=FACE_BOUND ( 'NONE', #27768, .T. ) ;
#26814=DIRECTION ( 'NONE',  ( 0.000000000000000000, 0.000000000000000000, 1.000000000000000000 ) ) ;
#26891=AXIS2_PLACEMENT_3D ( 'NONE', #48694, #26506, #60733 ) ;
#26900=( NAMED_UNIT ( * ) SI_UNIT ( $, .STERADIAN. ) SOLID_ANGLE_UNIT ( ) );
#26979=ORIENTED_EDGE ( 'NONE', *, *, #71614, .F. ) ;
#27001=CARTESIAN_POINT ( 'NONE',  ( 1.560000000000000053, 0.8660254037844389297, -1.500000000000000000 ) ) ;
#27155=ORIENTED_EDGE ( 'NONE', *, *, #26321, .T. ) ;
#27264=CARTESIAN_POINT ( 'NONE',  ( 1.560000000000000053, -0.8660254037844384856, -1.500000000000000000 ) ) ;
#27356=CARTESIAN_POINT ( 'NONE',  ( 4.755015822784811164, -4.336808689942017736E-16, 0.000000000000000000 ) ) ;
#27467=VECTOR ( 'NONE', #31266, 1000.000000000000000 ) ;
#27536=CARTESIAN_POINT ( 'NONE',  ( 22.75000000000000000, 0.000000000000000000, 2.055000000000000160 ) ) ;
#27689=EDGE_CURVE ( 'NONE', #68126, #12127, #53736, .T. ) ;
#27699=CARTESIAN_POINT ( 'NONE',  ( 2.750000000000000000, 0.000000000000000000, 0.000000000000000000 ) ) ;
#27768=EDGE_LOOP ( 'NONE', ( #19813, #63355 ) ) ;
#27908=LINE ( 'NONE', #5743, #67259 ) ;
#27917=ORIENTED_EDGE ( 'NONE', *, *, #28839, .T. ) ;
#27932=CYLINDRICAL_SURFACE ( 'NONE', #43829, 4.750000000000000000 ) ;
#27948=DIRECTION ( 'NONE',  ( 0.000000000000000000, 0.000000000000000000, 1.000000000000000000 ) ) ;
#28020=EDGE_CURVE ( 'NONE', #39761, #44032, #50127, .T. ) ;
#28107=DIRECTION ( 'NONE',  ( 0.000000000000000000, 1.000000000000000000, 0.000000000000000000 ) ) ;
#28116=AXIS2_PLACEMENT_3D ( 'NONE', #19440, #19070, #1830 ) ;
#28494=EDGE_CURVE ( 'NONE', #44032, #6380, #41835, .T. ) ;
#28552=CARTESIAN_POINT ( 'NONE',  ( 1.560000000000000053, -0.8660254037844384856, -1.500000000000000000 ) ) ;
#28584=ORIENTED_EDGE ( 'NONE', *, *, #46017, .T. ) ;
#28648=ORIENTED_EDGE ( 'NONE', *, *, #41516, .F. ) ;
#28667=ADVANCED_FACE ( 'NONE', ( #21479 ), #44442, .F. ) ;
#28671=DIRECTION ( 'NONE',  ( -1.000000000000000000, 0.000000000000000000, 0.000000000000000000 ) ) ;
#28737=AXIS2_PLACEMENT_3D ( 'NONE', #37940, #65772, #14631 ) ;
#28753=VERTEX_POINT ( 'NONE', #57572 ) ;
#28839=EDGE_CURVE ( 'NONE', #13145, #61765, #7173, .T. ) ;
#28883=EDGE_CURVE ( 'NONE', #1244, #13145, #65066, .T. ) ;
#28934=VERTEX_POINT ( 'NONE', #48132 ) ;
#28954=AXIS2_PLACEMENT_3D ( 'NONE', #63669, #12138, #69660 ) ;
#28983=CARTESIAN_POINT ( 'NONE',  ( 1.560000000000000053, 0.000000000000000000, 2.999999999999998668 ) ) ;
#29006=DIRECTION ( 'NONE',  ( 0.000000000000000000, 0.000000000000000000, 1.000000000000000000 ) ) ;
#29101=CARTESIAN_POINT ( 'NONE',  ( 2.949999999999999734, 0.000000000000000000, 0.000000000000000000 ) ) ;
#29231=ORIENTED_EDGE ( 'NONE', *, *, #5810, .F. ) ;
#29367=CARTESIAN_POINT ( 'NONE',  ( -997.5739745962155212, 0.000000000000000000, 0.000000000000000000 ) ) ;
#29460=CIRCLE ( 'NONE', #23473, 1.500000000000000000 ) ;
#29498=EDGE_CURVE ( 'NONE', #2397, #70414, #26193, .T. ) ;
#29533=CARTESIAN_POINT ( 'NONE',  ( 1.560000000000000053, 0.8660254037844389297, 1.500000000000000000 ) ) ;
#29607=ORIENTED_EDGE ( 'NONE', *, *, #56543, .F. ) ;
#29680=ORIENTED_EDGE ( 'NONE', *, *, #64868, .F. ) ;
#29747=ADVANCED_FACE ( 'NONE', ( #18268 ), #64510, .T. ) ;
#29867=CIRCLE ( 'NONE', #58696, 1.500000000000000000 ) ;
#30056=VECTOR ( 'NONE', #33705, 1000.000000000000000 ) ;
#30084=DIRECTION ( 'NONE',  ( -0.000000000000000000, -0.5000000000000003331, -0.8660254037844384856 ) ) ;
#30136=ORIENTED_EDGE ( 'NONE', *, *, #43894, .T. ) ;
#30197=PRODUCT_DEFINITION ( 'UNKNOWN', '', #18402, #31014 ) ;
#30304=CARTESIAN_POINT ( 'NONE',  ( 1.560000000000000053, 0.8660254037844389297, -1.500000000000000000 ) ) ;
#30662=ORIENTED_EDGE ( 'NONE', *, *, #7641, .F. ) ;
#30743=ORIENTED_EDGE ( 'NONE', *, *, #48123, .T. ) ;
#31014=PRODUCT_DEFINITION_CONTEXT ( 'detailed design', #72439, 'design' ) ;
#31098=VECTOR ( 'NONE', #49120, 1000.000000000000000 ) ;
#31189=LINE ( 'NONE', #37950, #71553 ) ;
#31207=AXIS2_PLACEMENT_3D ( 'NONE', #53949, #9180, #60336 ) ;
#31212=EDGE_CURVE ( 'NONE', #26602, #2572, #61196, .T. ) ;
#31260=DIRECTION ( 'NONE',  ( 1.000000000000000000, 0.000000000000000000, -0.000000000000000000 ) ) ;
#31266=DIRECTION ( 'NONE',  ( -0.000000000000000000, 1.000000000000000000, -0.000000000000000000 ) ) ;
#31366=FACE_OUTER_BOUND ( 'NONE', #45339, .T. ) ;
#31385=DIRECTION ( 'NONE',  ( 0.000000000000000000, 0.000000000000000000, 1.000000000000000000 ) ) ;
#31577=ADVANCED_FACE ( 'NONE', ( #6101 ), #22300, .F. ) ;
#31643=ADVANCED_FACE ( 'NONE', ( #43912 ), #22356, .F. ) ;
#31673=CIRCLE ( 'NONE', #26891, 2.500000000000000444 ) ;
#31674=DIRECTION ( 'NONE',  ( 0.000000000000000000, 0.000000000000000000, 1.000000000000000000 ) ) ;
#31778=ORIENTED_EDGE ( 'NONE', *, *, #28020, .T. ) ;
#31819=CARTESIAN_POINT ( 'NONE',  ( 0.000000000000000000, 0.8660254037844389297, -1.500000000000000000 ) ) ;
#31865=CARTESIAN_POINT ( 'NONE',  ( -997.5739745962155212, 0.000000000000000000, 0.000000000000000000 ) ) ;
#31886=AXIS2_PLACEMENT_3D ( 'NONE', #29367, #58322, #29006 ) ;
#31949=VECTOR ( 'NONE', #64316, 1000.000000000000000 ) ;
#31992=VERTEX_POINT ( 'NONE', #17547 ) ;
#32015=EDGE_CURVE ( 'NONE', #52268, #61765, #49450, .T. ) ;
#32029=CARTESIAN_POINT ( 'NONE',  ( 0.000000000000000000, 1.732050807568878747, 7.017607234860990640E-28 ) ) ;
#32035=DIRECTION ( 'NONE',  ( -1.000000000000000000, -0.000000000000000000, -0.000000000000000000 ) ) ;
#32146=AXIS2_PLACEMENT_3D ( 'NONE', #2493, #14460, #42667 ) ;
#32274=ORIENTED_EDGE ( 'NONE', *, *, #40910, .F. ) ;
#32297=CIRCLE ( 'NONE', #64732, 2.055000000000000160 ) ;
#32302=AXIS2_PLACEMENT_3D ( 'NONE', #54945, #3465, #9820 ) ;
#32414=AXIS2_PLACEMENT_3D ( 'NONE', #38511, #4691, #21577 ) ;
#32416=CIRCLE ( 'NONE', #22737, 4.750000000000000000 ) ;
#32605=CARTESIAN_POINT ( 'NONE',  ( 0.000000000000000000, 1.732050807568878747, 7.017607234860990640E-28 ) ) ;
#32730=EDGE_CURVE ( 'NONE', #14729, #2397, #56116, .T. ) ;
#32773=DIRECTION ( 'NONE',  ( 0.000000000000000000, 0.000000000000000000, 1.000000000000000000 ) ) ;
#32902=EDGE_LOOP ( 'NONE', ( #59916, #36723, #6163, #63248, #9146 ) ) ;
#32990=ORIENTED_EDGE ( 'NONE', *, *, #5792, .F. ) ;
#33110=DIRECTION ( 'NONE',  ( -0.000000000000000000, 0.000000000000000000, 1.000000000000000000 ) ) ;
#33272=EDGE_CURVE ( 'NONE', #28934, #68126, #412, .T. ) ;
#33331=ADVANCED_FACE ( 'NONE', ( #7486, #20228 ), #71354, .T. ) ;
#33391=CARTESIAN_POINT ( 'NONE',  ( 1.560000000000000053, -0.8660254037844384856, -1.500000000000000000 ) ) ;
#33525=SHAPE_REPRESENTATION ( 'socket button head screw_iso_ISO 7380 - M5 x 20 - 20N', ( #43395 ), #56756 ) ;
#33705=DIRECTION ( 'NONE',  ( -1.000000000000000000, 0.000000000000000000, 0.000000000000000000 ) ) ;
#33792=CIRCLE ( 'NONE', #20590, 2.375000000000000444 ) ;
#33850=ADVANCED_FACE ( 'NONE', ( #14422 ), #70761, .T. ) ;
#33918=COLOUR_RGB ( '', 0.31764706, 0.68627451, 0.89019608) ;
#33983=DIRECTION ( 'NONE',  ( 0.000000000000000000, 1.000000000000000000, 0.000000000000000000 ) ) ;
#34009=EDGE_LOOP ( 'NONE', ( #60704, #67577, #20443, #12843, #67504 ) ) ;
#34046=AXIS2_PLACEMENT_3D ( 'NONE', #59059, #54161, #2692 ) ;
#34252=DIRECTION ( 'NONE',  ( -1.000000000000000000, 0.000000000000000000, -0.000000000000000000 ) ) ;
#34314=AXIS2_PLACEMENT_3D ( 'NONE', #31865, #72456, #47776 ) ;
#34316=PLANE ( 'NONE',  #47574 ) ;
#34393=EDGE_LOOP ( 'NONE', ( #26979, #58089, #30136, #64360, #20429 ) ) ;
#34488=DIRECTION ( 'NONE',  ( 0.000000000000000000, 0.000000000000000000, -1.000000000000000000 ) ) ;
#34520=CARTESIAN_POINT ( 'NONE',  ( 22.75000000000000000, 0.000000000000000000, 0.000000000000000000 ) ) ;
#34800=CIRCLE ( 'NONE', #32414, 2.499999999999999556 ) ;
#35164=DIRECTION ( 'NONE',  ( 0.000000000000000000, -0.8660254037844384856, 0.5000000000000004441 ) ) ;
#35227=EDGE_LOOP ( 'NONE', ( #30743, #56332 ) ) ;
#35294=ADVANCED_FACE ( 'NONE', ( #64983 ), #53682, .T. ) ;
#35429=CARTESIAN_POINT ( 'NONE',  ( 0.000000000000000000, 0.000000000000000000, 2.499999999999999556 ) ) ;
#35512=SURFACE_STYLE_USAGE ( .BOTH. , #12205 ) ;
#35530=CARTESIAN_POINT ( 'NONE',  ( 1.560000000000000053, 1.732050807568878747, 7.017607234860990640E-28 ) ) ;
#35596=DIRECTION ( 'NONE',  ( 0.000000000000000000, 0.000000000000000000, 1.000000000000000000 ) ) ;
#35695=EDGE_LOOP ( 'NONE', ( #52893, #35776, #59931, #19952, #12384 ) ) ;
#35776=ORIENTED_EDGE ( 'NONE', *, *, #7641, .T. ) ;
#35872=FILL_AREA_STYLE_COLOUR ( '', #33918 ) ;
#35971=ORIENTED_EDGE ( 'NONE', *, *, #31212, .F. ) ;
#36065=ORIENTED_EDGE ( 'NONE', *, *, #41516, .T. ) ;
#36370=CARTESIAN_POINT ( 'NONE',  ( 1.560000000000000053, -1.299038105676658450, 0.7500000000000007772 ) ) ;
#36531=CARTESIAN_POINT ( 'NONE',  ( 1.560000000000000053, 0.8660254037844389297, -1.500000000000000000 ) ) ;
#36723=ORIENTED_EDGE ( 'NONE', *, *, #72097, .T. ) ;
#36889=MANIFOLD_SOLID_BREP ( 'Hex', #54797 ) ;
#37186=ORIENTED_EDGE ( 'NONE', *, *, #33272, .F. ) ;
#37264=ADVANCED_BREP_SHAPE_REPRESENTATION ( '', ( #36889, #43395 ), #56756 ) ;
#37408=ORIENTED_EDGE ( 'NONE', *, *, #58638, .F. ) ;
#37491=VECTOR ( 'NONE', #72885, 1000.000000000000000 ) ;
#37655=AXIS2_PLACEMENT_3D ( 'NONE', #27699, #50623, #5163 ) ;
#37669=PLANE ( 'NONE',  #1127 ) ;
#37940=CARTESIAN_POINT ( 'NONE',  ( 2.369999999999999662, 0.000000000000000000, 0.000000000000000000 ) ) ;
#37950=CARTESIAN_POINT ( 'NONE',  ( 0.000000000000000000, -0.8660254037844384856, 1.500000000000000000 ) ) ;
#38118=DIRECTION ( 'NONE',  ( -1.000000000000000000, -0.000000000000000000, -0.000000000000000000 ) ) ;
#38278=VECTOR ( 'NONE', #24457, 1000.000000000000000 ) ;
#38401=DIRECTION ( 'NONE',  ( -1.000000000000000000, 0.000000000000000000, -0.000000000000000000 ) ) ;
#38433=CARTESIAN_POINT ( 'NONE',  ( 2.369999999999999662, 0.000000000000000000, 0.000000000000000000 ) ) ;
#38437=ORIENTED_EDGE ( 'NONE', *, *, #28839, .F. ) ;
#38511=CARTESIAN_POINT ( 'NONE',  ( 2.949999999999999734, 0.000000000000000000, 0.000000000000000000 ) ) ;
#38612=DIRECTION ( 'NONE',  ( 0.000000000000000000, 0.000000000000000000, 1.000000000000000000 ) ) ;
#38693=DIRECTION ( 'NONE',  ( 0.000000000000000000, 0.000000000000000000, 1.000000000000000000 ) ) ;
#38722=PRESENTATION_STYLE_ASSIGNMENT (( #4525 ) ) ;
#38824=DIRECTION ( 'NONE',  ( -1.000000000000000000, -0.000000000000000000, -0.000000000000000000 ) ) ;
#38935=CIRCLE ( 'NONE', #12526, 5.315148208181397216 ) ;
#38942=CARTESIAN_POINT ( 'NONE',  ( 1.560000000000000053, 0.000000000000000000, 0.000000000000000000 ) ) ;
#39076=CARTESIAN_POINT ( 'NONE',  ( 0.000000000000000000, -2.375000000000000444, -4.362804221962445569E-16 ) ) ;
#39087=VECTOR ( 'NONE', #24605, 1000.000000000000114 ) ;
#39142=CARTESIAN_POINT ( 'NONE',  ( 2.750000000000000000, 2.499999999999999112, 0.000000000000000000 ) ) ;
#39179=CARTESIAN_POINT ( 'NONE',  ( 22.30499999999999972, 3.061616997868384127E-16, -2.500000000000000888 ) ) ;
#39249=DIRECTION ( 'NONE',  ( -0.000000000000000000, 0.5000000000000003331, -0.8660254037844384856 ) ) ;
#39427=EDGE_LOOP ( 'NONE', ( #21921, #54559, #68218, #43502 ) ) ;
#39447=DIRECTION ( 'NONE',  ( -1.000000000000000000, -0.000000000000000000, -0.000000000000000000 ) ) ;
#39695=DIRECTION ( 'NONE',  ( -1.000000000000000000, -0.000000000000000000, -0.000000000000000000 ) ) ;
#39761=VERTEX_POINT ( 'NONE', #19958 ) ;
#39971=CARTESIAN_POINT ( 'NONE',  ( 1.560000000000000053, -0.8660254037844384856, -1.500000000000000000 ) ) ;
#40295=FACE_OUTER_BOUND ( 'NONE', #46318, .T. ) ;
#40355=ORIENTED_EDGE ( 'NONE', *, *, #49960, .F. ) ;
#40410=( NAMED_UNIT ( * ) SI_UNIT ( $, .STERADIAN. ) SOLID_ANGLE_UNIT ( ) );
#40610=ORIENTED_EDGE ( 'NONE', *, *, #28020, .F. ) ;
#40822=ORIENTED_EDGE ( 'NONE', *, *, #29498, .F. ) ;
#40854=VERTEX_POINT ( 'NONE', #31819 ) ;
#40910=EDGE_CURVE ( 'NONE', #1244, #57811, #15663, .T. ) ;
#41113=DIRECTION ( 'NONE',  ( -0.000000000000000000, -0.5000000000000003331, -0.8660254037844384856 ) ) ;
#41190=EDGE_CURVE ( 'NONE', #14148, #23851, #9594, .T. ) ;
#41406=ADVANCED_FACE ( 'NONE', ( #31366 ), #20832, .T. ) ;
#41437=DIRECTION ( 'NONE',  ( 0.000000000000000000, 0.000000000000000000, 1.000000000000000000 ) ) ;
#41516=EDGE_CURVE ( 'NONE', #72658, #31992, #4677, .T. ) ;
#41775=EDGE_LOOP ( 'NONE', ( #3825, #3011 ) ) ;
#41835=LINE ( 'NONE', #71872, #68234 ) ;
#41897=FILL_AREA_STYLE ('',( #35872 ) ) ;
#42040=CARTESIAN_POINT ( 'NONE',  ( 2.369999999999999662, 0.000000000000000000, 4.750000000000000000 ) ) ;
#42314=ORIENTED_EDGE ( 'NONE', *, *, #14147, .T. ) ;
#42323=DIRECTION ( 'NONE',  ( 0.000000000000000000, -0.8660254037844384856, -0.5000000000000004441 ) ) ;
#42409=CARTESIAN_POINT ( 'NONE',  ( 1.560000000000000053, -0.8660254037844384856, 1.500000000000000000 ) ) ;
#42667=DIRECTION ( 'NONE',  ( 0.000000000000000000, 0.000000000000000000, 1.000000000000000000 ) ) ;
#42792=AXIS2_PLACEMENT_3D ( 'NONE', #19974, #65495, #60232 ) ;
#42826=ORIENTED_EDGE ( 'NONE', *, *, #1316, .T. ) ;
#42913=DIRECTION ( 'NONE',  ( 0.000000000000000000, -1.000000000000000000, 0.000000000000000000 ) ) ;
#42946=DIRECTION ( 'NONE',  ( 0.000000000000000000, 0.000000000000000000, 1.000000000000000000 ) ) ;
#43004=CARTESIAN_POINT ( 'NONE',  ( 22.75000000000000000, 0.000000000000000000, 0.000000000000000000 ) ) ;
#43089=CARTESIAN_POINT ( 'NONE',  ( 1.560000000000000053, 0.8660254037844389297, 1.500000000000000000 ) ) ;
#43264=CYLINDRICAL_SURFACE ( 'NONE', #34046, 2.499999999999999556 ) ;
#43310=CARTESIAN_POINT ( 'NONE',  ( 2.369999999999999662, 5.817072295949927426E-16, -4.750000000000000000 ) ) ;
#43395=AXIS2_PLACEMENT_3D ( 'NONE', #48320, #71232, #19735 ) ;
#43424=CONICAL_SURFACE ( 'NONE', #73376, 2.055000000000000160, 0.7853981633974479459 ) ;
#43461=VERTEX_POINT ( 'NONE', #7179 ) ;
#43493=CARTESIAN_POINT ( 'NONE',  ( 0.000000000000000000, 0.8660254037844389297, -1.500000000000000000 ) ) ;
#43502=ORIENTED_EDGE ( 'NONE', *, *, #51809, .F. ) ;
#43770=ORIENTED_EDGE ( 'NONE', *, *, #33272, .T. ) ;
#43801=EDGE_CURVE ( 'NONE', #23851, #68126, #29867, .T. ) ;
#43823=ORIENTED_EDGE ( 'NONE', *, *, #66718, .F. ) ;
#43829=AXIS2_PLACEMENT_3D ( 'NONE', #55394, #3915, #26814 ) ;
#43884=VECTOR ( 'NONE', #49161, 1000.000000000000000 ) ;
#43894=EDGE_CURVE ( 'NONE', #6380, #70995, #11832, .T. ) ;
#43912=FACE_OUTER_BOUND ( 'NONE', #34009, .T. ) ;
#44032=VERTEX_POINT ( 'NONE', #62878 ) ;
#44076=CIRCLE ( 'NONE', #11643, 2.055000000000000160 ) ;
#44304=ORIENTED_EDGE ( 'NONE', *, *, #46619, .T. ) ;
#44442=PLANE ( 'NONE',  #56271 ) ;
#44767=CARTESIAN_POINT ( 'NONE',  ( 1.560000000000000053, 1.299038105676658228, -0.7500000000000009992 ) ) ;
#44837=EDGE_LOOP ( 'NONE', ( #25595, #42826, #6045, #38437, #67542 ) ) ;
#44868=PRODUCT_CONTEXT ( 'NONE', #61373, 'mechanical' ) ;
#45050=ORIENTED_EDGE ( 'NONE', *, *, #46017, .F. ) ;
#45150=EDGE_CURVE ( 'NONE', #6105, #19678, #58873, .T. ) ;
#45339=EDGE_LOOP ( 'NONE', ( #5571, #25135, #49101 ) ) ;
#45346=ADVANCED_FACE ( 'NONE', ( #40295 ), #69237, .T. ) ;
#45476=COLOUR_RGB ( '', 0.31764706, 0.68627451, 0.89019608) ;
#45572=VECTOR ( 'NONE', #51493, 1000.000000000000114 ) ;
#45710=( LENGTH_UNIT ( ) NAMED_UNIT ( * ) SI_UNIT ( .MILLI., .METRE. ) );
#45954=ORIENTED_EDGE ( 'NONE', *, *, #41190, .F. ) ;
#45985=DIRECTION ( 'NONE',  ( 0.000000000000000000, 0.000000000000000000, 1.000000000000000000 ) ) ;
#46017=EDGE_CURVE ( 'NONE', #57811, #14148, #13176, .T. ) ;
#46018=( GEOMETRIC_REPRESENTATION_CONTEXT ( 3 ) GLOBAL_UNCERTAINTY_ASSIGNED_CONTEXT ( ( #71605 ) ) GLOBAL_UNIT_ASSIGNED_CONTEXT ( ( #57337, #602, #40410 ) ) REPRESENTATION_CONTEXT ( 'NONE', 'WORKASPACE' ) );
#46318=EDGE_LOOP ( 'NONE', ( #22291, #37408, #63173 ) ) ;
#46421=EDGE_CURVE ( 'NONE', #26602, #43461, #55254, .T. ) ;
#46501=DIRECTION ( 'NONE',  ( -1.000000000000000000, 0.000000000000000000, 0.000000000000000000 ) ) ;
#46545=FACE_OUTER_BOUND ( 'NONE', #20036, .T. ) ;
#46619=EDGE_CURVE ( 'NONE', #28753, #59706, #1273, .T. ) ;
#46710=VERTEX_POINT ( 'NONE', #39971 ) ;
#47023=CARTESIAN_POINT ( 'NONE',  ( 2.369999999999999662, -4.750000000000000888, -5.817072295949926440E-16 ) ) ;
#47202=VECTOR ( 'NONE', #46501, 1000.000000000000000 ) ;
#47461=ORIENTED_EDGE ( 'NONE', *, *, #22833, .T. ) ;
#47558=EDGE_LOOP ( 'NONE', ( #43770, #22828, #13778, #28648, #40355 ) ) ;
#47574=AXIS2_PLACEMENT_3D ( 'NONE', #5765, #28671, #45985 ) ;
#47623=DIRECTION ( 'NONE',  ( -1.000000000000000000, -0.000000000000000000, -0.000000000000000000 ) ) ;
#47776=DIRECTION ( 'NONE',  ( 0.000000000000000000, 0.000000000000000000, 1.000000000000000000 ) ) ;
#47948=ADVANCED_FACE ( 'NONE', ( #6875 ), #43424, .T. ) ;
#47957=EDGE_CURVE ( 'NONE', #2572, #26602, #55416, .T. ) ;
#48022=EDGE_LOOP ( 'NONE', ( #21434, #31778, #72478, #22650, #66863 ) ) ;
#48123=EDGE_CURVE ( 'NONE', #19678, #6105, #33792, .T. ) ;
#48132=CARTESIAN_POINT ( 'NONE',  ( 1.560000000000000053, -1.732050807568877859, -1.752539433813135784E-17 ) ) ;
#48320=CARTESIAN_POINT ( 'NONE',  ( 0.000000000000000000, 0.000000000000000000, 0.000000000000000000 ) ) ;
#48413=DIRECTION ( 'NONE',  ( 0.000000000000000000, 0.000000000000000000, -1.000000000000000000 ) ) ;
#48451=VERTEX_POINT ( 'NONE', #23706 ) ;
#48578=CARTESIAN_POINT ( 'NONE',  ( 0.000000000000000000, 0.000000000000000000, 0.000000000000000000 ) ) ;
#48694=CARTESIAN_POINT ( 'NONE',  ( 22.30499999999999972, 0.000000000000000000, 0.000000000000000000 ) ) ;
#48774=DIRECTION ( 'NONE',  ( 0.000000000000000000, 0.000000000000000000, 1.000000000000000000 ) ) ;
#49101=ORIENTED_EDGE ( 'NONE', *, *, #53507, .F. ) ;
#49120=DIRECTION ( 'NONE',  ( -0.000000000000000000, -0.5000000000000004441, 0.8660254037844383745 ) ) ;
#49151=CARTESIAN_POINT ( 'NONE',  ( 1.560000000000000053, 1.732050807568878747, 7.017607234860990640E-28 ) ) ;
#49161=DIRECTION ( 'NONE',  ( -0.000000000000000000, 0.5000000000000004441, 0.8660254037844383745 ) ) ;
#49365=PRODUCT ( 'socket button head screw_iso_ISO 7380 - M5 x 20 - 20N', 'socket button head screw_iso_ISO 7380 - M5 x 20 - 20N', '', ( #44868 ) ) ;
#49450=LINE ( 'NONE', #43089, #2340 ) ;
#49531=TOROIDAL_SURFACE ( 'NONE', #23165, 2.699999999999999734, 0.2000000000000000111 ) ;
#49744=DIRECTION ( 'NONE',  ( -0.000000000000000000, 1.000000000000000000, 1.224646799147353207E-16 ) ) ;
#49862=TOROIDAL_SURFACE ( 'NONE', #61910, 2.699999999999999734, 0.2000000000000000111 ) ;
#49899=ORIENTED_EDGE ( 'NONE', *, *, #19913, .F. ) ;
#49960=EDGE_CURVE ( 'NONE', #28934, #72658, #2947, .T. ) ;
#49963=CARTESIAN_POINT ( 'NONE',  ( 0.000000000000000000, 3.061616997868382648E-16, -2.499999999999999556 ) ) ;
#50104=LINE ( 'NONE', #61038, #12590 ) ;
#50127=CIRCLE ( 'NONE', #32146, 4.750000000000000000 ) ;
#50130=ADVANCED_FACE ( 'NONE', ( #62293 ), #17161, .T. ) ;
#50217=CARTESIAN_POINT ( 'NONE',  ( 0.000000000000000000, -1.732050807568877859, -1.752539433813135784E-17 ) ) ;
#50361=AXIS2_PLACEMENT_3D ( 'NONE', #33391, #4870, #22131 ) ;
#50383=ORIENTED_EDGE ( 'NONE', *, *, #49960, .T. ) ;
#50430=EDGE_CURVE ( 'NONE', #70995, #19678, #38935, .T. ) ;
#50469=DIRECTION ( 'NONE',  ( -0.7071067811865479058, 0.000000000000000000, 0.7071067811865472397 ) ) ;
#50569=EDGE_LOOP ( 'NONE', ( #11918, #16548, #40822, #23953 ) ) ;
#50623=DIRECTION ( 'NONE',  ( -1.000000000000000000, -0.000000000000000000, -0.000000000000000000 ) ) ;
#50731=EDGE_CURVE ( 'NONE', #17476, #28753, #53133, .T. ) ;
#50980=CARTESIAN_POINT ( 'NONE',  ( 1.560000000000000053, 0.000000000000000000, 0.000000000000000000 ) ) ;
#50994=AXIS2_PLACEMENT_3D ( 'NONE', #27356, #34488, #28107 ) ;
#51012=ORIENTED_EDGE ( 'NONE', *, *, #64167, .T. ) ;
#51070=FACE_OUTER_BOUND ( 'NONE', #47558, .T. ) ;
#51249=DIRECTION ( 'NONE',  ( -1.000000000000000000, -0.000000000000000000, -0.000000000000000000 ) ) ;
#51287=ADVANCED_FACE ( 'NONE', ( #8664 ), #43264, .T. ) ;
#51493=DIRECTION ( 'NONE',  ( -0.000000000000000000, 0.5000000000000003331, -0.8660254037844384856 ) ) ;
#51495=ORIENTED_EDGE ( 'NONE', *, *, #10504, .F. ) ;
#51606=AXIS2_PLACEMENT_3D ( 'NONE', #50980, #70847, #8072 ) ;
#51633=CARTESIAN_POINT ( 'NONE',  ( 0.000000000000000000, -0.8660254037844384856, -1.500000000000000000 ) ) ;
#51809=EDGE_CURVE ( 'NONE', #70414, #2397, #31673, .T. ) ;
#51917=DIRECTION ( 'NONE',  ( 0.000000000000000000, 0.000000000000000000, 1.000000000000000000 ) ) ;
#51919=ORIENTED_EDGE ( 'NONE', *, *, #51809, .T. ) ;
#51945=EDGE_CURVE ( 'NONE', #39761, #59464, #21976, .T. ) ;
#51946=EDGE_LOOP ( 'NONE', ( #58223, #51919, #27155, #71702 ) ) ;
#52028=CIRCLE ( 'NONE', #37655, 4.750000000000000000 ) ;
#52039=ADVANCED_FACE ( 'NONE', ( #571 ), #18914, .T. ) ;
#52064=CARTESIAN_POINT ( 'NONE',  ( 1.560000000000000053, -1.732050807568877859, -1.752539433813135784E-17 ) ) ;
#52268=VERTEX_POINT ( 'NONE', #73374 ) ;
#52442=AXIS2_PLACEMENT_3D ( 'NONE', #71455, #42913, #15817 ) ;
#52473=DIRECTION ( 'NONE',  ( 0.000000000000000000, 0.5000000000000003331, -0.8660254037844383745 ) ) ;
#52696=ORIENTED_EDGE ( 'NONE', *, *, #68496, .T. ) ;
#52722=DIRECTION ( 'NONE',  ( -1.000000000000000000, -0.000000000000000000, -0.000000000000000000 ) ) ;
#52893=ORIENTED_EDGE ( 'NONE', *, *, #5792, .T. ) ;
#53011=VERTEX_POINT ( 'NONE', #62796 ) ;
#53133=LINE ( 'NONE', #68954, #70104 ) ;
#53142=MECHANICAL_DESIGN_GEOMETRIC_PRESENTATION_REPRESENTATION('',(#1561),#46018);
#53146=ADVANCED_FACE ( 'NONE', ( #72779 ), #49862, .F. ) ;
#53250=DIRECTION ( 'NONE',  ( -0.000000000000000000, 1.000000000000000000, -0.000000000000000000 ) ) ;
#53268=CARTESIAN_POINT ( 'NONE',  ( 0.000000000000000000, 0.000000000000000000, 0.000000000000000000 ) ) ;
#53315=AXIS2_PLACEMENT_3D ( 'NONE', #23831, #70048, #12173 ) ;
#53507=EDGE_CURVE ( 'NONE', #28753, #57811, #29460, .T. ) ;
#53682=PLANE ( 'NONE',  #19353 ) ;
#53736=CIRCLE ( 'NONE', #17721, 1.500000000000000000 ) ;
#53806=ORIENTED_EDGE ( 'NONE', *, *, #46619, .F. ) ;
#53813=MECHANICAL_DESIGN_GEOMETRIC_PRESENTATION_REPRESENTATION('',(#58649),#2233);
#53895=EDGE_LOOP ( 'NONE', ( #32990, #29680, #45954 ) ) ;
#53949=CARTESIAN_POINT ( 'NONE',  ( 1.560000000000000053, 0.000000000000000000, 2.999999999999998668 ) ) ;
#53994=CARTESIAN_POINT ( 'NONE',  ( 1.560000000000000053, 0.000000000000000000, 0.000000000000000000 ) ) ;
#54149=CARTESIAN_POINT ( 'NONE',  ( 0.000000000000000000, 0.8660254037844389297, 1.500000000000000000 ) ) ;
#54161=DIRECTION ( 'NONE',  ( -1.000000000000000000, -0.000000000000000000, -0.000000000000000000 ) ) ;
#54214=CARTESIAN_POINT ( 'NONE',  ( 22.75000000000000000, 0.000000000000000000, 0.000000000000000000 ) ) ;
#54334=CARTESIAN_POINT ( 'NONE',  ( 4.755015822784811164, -4.336808689942017736E-16, 0.000000000000000000 ) ) ;
#54419=CARTESIAN_POINT ( 'NONE',  ( 22.30499999999999972, 0.000000000000000000, 0.000000000000000000 ) ) ;
#54452=CARTESIAN_POINT ( 'NONE',  ( 0.000000000000000000, 0.000000000000000000, 0.000000000000000000 ) ) ;
#54559=ORIENTED_EDGE ( 'NONE', *, *, #64917, .T. ) ;
#54797=CLOSED_SHELL ( 'NONE', ( #31643, #23434, #33850, #25464, #59164, #25324, #33331, #68065, #52039, #63609, #51287, #47948, #28667, #53146, #26500, #10787, #20197, #18821, #29747, #35294, #41406, #7461, #26474, #45346, #50130, #22438, #31577 ) ) ;
#54945=CARTESIAN_POINT ( 'NONE',  ( 2.949999999999999734, 0.000000000000000000, 0.000000000000000000 ) ) ;
#55120=CIRCLE ( 'NONE', #32302, 2.499999999999999556 ) ;
#55162=CARTESIAN_POINT ( 'NONE',  ( 1.560000000000000053, 0.8660254037844389297, 1.500000000000000000 ) ) ;
#55180=CIRCLE ( 'NONE', #25195, 5.315148208181396328 ) ;
#55254=CIRCLE ( 'NONE', #73218, 0.2000000000000000944 ) ;
#55306=EDGE_LOOP ( 'NONE', ( #20752, #58818, #50383, #6343, #49899 ) ) ;
#55394=CARTESIAN_POINT ( 'NONE',  ( 0.000000000000000000, 0.000000000000000000, 0.000000000000000000 ) ) ;
#55416=CIRCLE ( 'NONE', #28954, 2.699999999999999734 ) ;
#55587=FACE_OUTER_BOUND ( 'NONE', #71269, .T. ) ;
#55722=CARTESIAN_POINT ( 'NONE',  ( 1.560000000000000053, 0.000000000000000000, 0.000000000000000000 ) ) ;
#56116=LINE ( 'NONE', #27536, #24996 ) ;
#56259=CARTESIAN_POINT ( 'NONE',  ( 2.949999999999999734, 0.000000000000000000, 0.000000000000000000 ) ) ;
#56271=AXIS2_PLACEMENT_3D ( 'NONE', #11321, #34252, #17705 ) ;
#56332=ORIENTED_EDGE ( 'NONE', *, *, #45150, .T. ) ;
#56342=DIRECTION ( 'NONE',  ( 0.000000000000000000, 0.000000000000000000, 1.000000000000000000 ) ) ;
#56392=SURFACE_SIDE_STYLE ('',( #21789 ) ) ;
#56543=EDGE_CURVE ( 'NONE', #44032, #39761, #52028, .T. ) ;
#56756=( GEOMETRIC_REPRESENTATION_CONTEXT ( 3 ) GLOBAL_UNCERTAINTY_ASSIGNED_CONTEXT ( ( #2508 ) ) GLOBAL_UNIT_ASSIGNED_CONTEXT ( ( #45710, #63008, #26900 ) ) REPRESENTATION_CONTEXT ( 'NONE', 'WORKASPACE' ) );
#56872=ORIENTED_EDGE ( 'NONE', *, *, #27689, .F. ) ;
#56960=AXIS2_PLACEMENT_3D ( 'NONE', #53268, #47623, #35596 ) ;
#57127=CARTESIAN_POINT ( 'NONE',  ( 22.30499999999999972, 0.000000000000000000, 2.500000000000000444 ) ) ;
#57181=EDGE_LOOP ( 'NONE', ( #62538, #2366, #42314, #21481 ) ) ;
#57227=LINE ( 'NONE', #24132, #68295 ) ;
#57231=CIRCLE ( 'NONE', #52442, 0.2000000000000000944 ) ;
#57275=DIRECTION ( 'NONE',  ( 0.000000000000000000, 0.000000000000000000, 1.000000000000000000 ) ) ;
#57285=LINE ( 'NONE', #552, #6047 ) ;
#57337=( LENGTH_UNIT ( ) NAMED_UNIT ( * ) SI_UNIT ( .MILLI., .METRE. ) );
#57467=DIRECTION ( 'NONE',  ( -1.000000000000000000, -0.000000000000000000, -0.000000000000000000 ) ) ;
#57572=CARTESIAN_POINT ( 'NONE',  ( 1.560000000000000053, 0.000000000000000000, 1.500000000000000000 ) ) ;
#57629=VECTOR ( 'NONE', #60086, 1000.000000000000000 ) ;
#57811=VERTEX_POINT ( 'NONE', #9491 ) ;
#57883=CARTESIAN_POINT ( 'NONE',  ( 1.560000000000000053, 0.000000000000000000, -1.499999999999999556 ) ) ;
#58084=LINE ( 'NONE', #52064, #39087 ) ;
#58089=ORIENTED_EDGE ( 'NONE', *, *, #8668, .T. ) ;
#58191=PLANE ( 'NONE',  #28116 ) ;
#58223=ORIENTED_EDGE ( 'NONE', *, *, #22833, .F. ) ;
#58298=CARTESIAN_POINT ( 'NONE',  ( 1.560000000000000053, 0.000000000000000000, 0.000000000000000000 ) ) ;
#58322=DIRECTION ( 'NONE',  ( -1.000000000000000000, -0.000000000000000000, -0.000000000000000000 ) ) ;
#58375=EDGE_CURVE ( 'NONE', #40854, #13145, #3698, .T. ) ;
#58530=CYLINDRICAL_SURFACE ( 'NONE', #56960, 2.499999999999999556 ) ;
#58638=EDGE_CURVE ( 'NONE', #68126, #46710, #73503, .T. ) ;
#58649=STYLED_ITEM ( 'NONE', ( #38722 ), #36889 ) ;
#58696=AXIS2_PLACEMENT_3D ( 'NONE', #55722, #32035, #31674 ) ;
#58763=AXIS2_PLACEMENT_3D ( 'NONE', #54452, #65377, #25147 ) ;
#58818=ORIENTED_EDGE ( 'NONE', *, *, #71785, .T. ) ;
#58873=CIRCLE ( 'NONE', #21605, 2.375000000000000444 ) ;
#59058=AXIS2_PLACEMENT_3D ( 'NONE', #28983, #68855, #51917 ) ;
#59059=CARTESIAN_POINT ( 'NONE',  ( 0.000000000000000000, 0.000000000000000000, 0.000000000000000000 ) ) ;
#59164=ADVANCED_FACE ( 'NONE', ( #10271 ), #27932, .T. ) ;
#59414=DIRECTION ( 'NONE',  ( -1.000000000000000000, 0.000000000000000000, 0.000000000000000000 ) ) ;
#59464=VERTEX_POINT ( 'NONE', #43310 ) ;
#59706=VERTEX_POINT ( 'NONE', #62829 ) ;
#59849=PLANE ( 'NONE',  #67665 ) ;
#59852=PLANE ( 'NONE',  #42792 ) ;
#59916=ORIENTED_EDGE ( 'NONE', *, *, #10504, .T. ) ;
#59931=ORIENTED_EDGE ( 'NONE', *, *, #28883, .T. ) ;
#60086=DIRECTION ( 'NONE',  ( -0.000000000000000000, -0.5000000000000004441, 0.8660254037844383745 ) ) ;
#60232=DIRECTION ( 'NONE',  ( 0.000000000000000000, 0.5000000000000003331, 0.8660254037844383745 ) ) ;
#60336=DIRECTION ( 'NONE',  ( 0.000000000000000000, 0.000000000000000000, 1.000000000000000000 ) ) ;
#60655=ORIENTED_EDGE ( 'NONE', *, *, #71785, .F. ) ;
#60704=ORIENTED_EDGE ( 'NONE', *, *, #50731, .F. ) ;
#60708=CARTESIAN_POINT ( 'NONE',  ( 1.560000000000000053, -0.8660254037844384856, 1.500000000000000000 ) ) ;
#60733=DIRECTION ( 'NONE',  ( 0.000000000000000000, 0.000000000000000000, 1.000000000000000000 ) ) ;
#61038=CARTESIAN_POINT ( 'NONE',  ( 1.560000000000000053, -0.8660254037844384856, 1.500000000000000000 ) ) ;
#61196=CIRCLE ( 'NONE', #10803, 2.699999999999999734 ) ;
#61221=VECTOR ( 'NONE', #23780, 1000.000000000000000 ) ;
#61286=( NAMED_UNIT ( * ) PLANE_ANGLE_UNIT ( ) SI_UNIT ( $, .RADIAN. ) );
#61373=APPLICATION_CONTEXT ( 'automotive_design' ) ;
#61500=EDGE_LOOP ( 'NONE', ( #68200, #44304, #68805, #43823, #223 ) ) ;
#61696=EDGE_CURVE ( 'NONE', #14729, #53011, #44076, .T. ) ;
#61764=DIRECTION ( 'NONE',  ( 0.000000000000000000, 0.000000000000000000, 1.000000000000000000 ) ) ;
#61765=VERTEX_POINT ( 'NONE', #24360 ) ;
#61787=SHAPE_DEFINITION_REPRESENTATION ( #26562, #33525 ) ;
#61790=DIRECTION ( 'NONE',  ( -1.000000000000000000, 0.000000000000000000, 0.000000000000000000 ) ) ;
#61819=DIRECTION ( 'NONE',  ( 0.000000000000000000, 1.000000000000000000, 1.224646799147353454E-16 ) ) ;
#61898=EDGE_LOOP ( 'NONE', ( #23843, #1920, #51495, #14245, #69875 ) ) ;
#61910=AXIS2_PLACEMENT_3D ( 'NONE', #56259, #62665, #11139 ) ;
#62293=FACE_OUTER_BOUND ( 'NONE', #19939, .T. ) ;
#62399=VECTOR ( 'NONE', #53250, 1000.000000000000000 ) ;
#62538=ORIENTED_EDGE ( 'NONE', *, *, #46421, .F. ) ;
#62545=CARTESIAN_POINT ( 'NONE',  ( 1.560000000000000053, -0.8660254037844384856, 1.500000000000000000 ) ) ;
#62665=DIRECTION ( 'NONE',  ( -1.000000000000000000, -0.000000000000000000, -0.000000000000000000 ) ) ;
#62796=CARTESIAN_POINT ( 'NONE',  ( 22.75000000000000000, 2.789133085058097101E-16, -2.055000000000000160 ) ) ;
#62829=CARTESIAN_POINT ( 'NONE',  ( 1.560000000000000053, -0.8660254037844384856, 1.500000000000000000 ) ) ;
#62839=ORIENTED_EDGE ( 'NONE', *, *, #63673, .F. ) ;
#62878=CARTESIAN_POINT ( 'NONE',  ( 2.750000000000000000, 0.000000000000000000, 4.750000000000000000 ) ) ;
#63008=( NAMED_UNIT ( * ) PLANE_ANGLE_UNIT ( ) SI_UNIT ( $, .RADIAN. ) );
#63173=ORIENTED_EDGE ( 'NONE', *, *, #43801, .F. ) ;
#63220=CIRCLE ( 'NONE', #7971, 1.500000000000000000 ) ;
#63240=EDGE_LOOP ( 'NONE', ( #35971, #20271, #62839, #14774 ) ) ;
#63248=ORIENTED_EDGE ( 'NONE', *, *, #48123, .F. ) ;
#63355=ORIENTED_EDGE ( 'NONE', *, *, #31212, .T. ) ;
#63470=EDGE_LOOP ( 'NONE', ( #5087, #53806, #29231 ) ) ;
#63609=ADVANCED_FACE ( 'NONE', ( #26732, #15456 ), #37669, .F. ) ;
#63669=CARTESIAN_POINT ( 'NONE',  ( 2.750000000000000000, 0.000000000000000000, 0.000000000000000000 ) ) ;
#63673=EDGE_CURVE ( 'NONE', #26241, #43461, #55120, .T. ) ;
#63687=DIRECTION ( 'NONE',  ( 0.000000000000000000, 0.000000000000000000, -1.000000000000000000 ) ) ;
#63712=FACE_OUTER_BOUND ( 'NONE', #63240, .T. ) ;
#63843=CARTESIAN_POINT ( 'NONE',  ( 22.75000000000000000, 0.000000000000000000, 2.055000000000000160 ) ) ;
#63868=DIRECTION ( 'NONE',  ( 0.000000000000000000, 0.000000000000000000, 1.000000000000000000 ) ) ;
#64167=EDGE_CURVE ( 'NONE', #46710, #23851, #9878, .T. ) ;
#64264=EDGE_CURVE ( 'NONE', #17476, #23851, #27908, .T. ) ;
#64316=DIRECTION ( 'NONE',  ( -0.000000000000000000, 0.5000000000000004441, 0.8660254037844383745 ) ) ;
#64360=ORIENTED_EDGE ( 'NONE', *, *, #50430, .T. ) ;
#64510=PLANE ( 'NONE',  #74183 ) ;
#64732=AXIS2_PLACEMENT_3D ( 'NONE', #54214, #72582, #25269 ) ;
#64743=ORIENTED_EDGE ( 'NONE', *, *, #73169, .T. ) ;
#64868=EDGE_CURVE ( 'NONE', #23851, #67138, #71844, .T. ) ;
#64917=EDGE_CURVE ( 'NONE', #53011, #14729, #32297, .T. ) ;
#64983=FACE_OUTER_BOUND ( 'NONE', #61500, .T. ) ;
#65066=LINE ( 'NONE', #13540, #15405 ) ;
#65148=EDGE_LOOP ( 'NONE', ( #21446, #25723, #69379, #28584, #66473 ) ) ;
#65377=DIRECTION ( 'NONE',  ( -1.000000000000000000, 0.000000000000000000, -0.000000000000000000 ) ) ;
#65495=DIRECTION ( 'NONE',  ( 0.000000000000000000, 0.8660254037844384856, -0.5000000000000004441 ) ) ;
#65571=DIRECTION ( 'NONE',  ( -1.000000000000000000, -0.000000000000000000, -0.000000000000000000 ) ) ;
#65630=ORIENTED_EDGE ( 'NONE', *, *, #73088, .T. ) ;
#65772=DIRECTION ( 'NONE',  ( -1.000000000000000000, -0.000000000000000000, -0.000000000000000000 ) ) ;
#66436=LINE ( 'NONE', #19806, #66551 ) ;
#66450=DIRECTION ( 'NONE',  ( -1.000000000000000000, -0.000000000000000000, -0.000000000000000000 ) ) ;
#66473=ORIENTED_EDGE ( 'NONE', *, *, #41190, .T. ) ;
#66551=VECTOR ( 'NONE', #26187, 1000.000000000000000 ) ;
#66718=EDGE_CURVE ( 'NONE', #61765, #48451, #31189, .T. ) ;
#66863=ORIENTED_EDGE ( 'NONE', *, *, #72097, .F. ) ;
#67006=DIRECTION ( 'NONE',  ( 0.000000000000000000, 0.000000000000000000, 1.000000000000000000 ) ) ;
#67137=LINE ( 'NONE', #43493, #72775 ) ;
#67138=VERTEX_POINT ( 'NONE', #24728 ) ;
#67259=VECTOR ( 'NONE', #74140, 1000.000000000000114 ) ;
#67504=ORIENTED_EDGE ( 'NONE', *, *, #5810, .T. ) ;
#67542=ORIENTED_EDGE ( 'NONE', *, *, #28883, .F. ) ;
#67577=ORIENTED_EDGE ( 'NONE', *, *, #64264, .T. ) ;
#67665=AXIS2_PLACEMENT_3D ( 'NONE', #27001, #41437, #31260 ) ;
#68065=ADVANCED_FACE ( 'NONE', ( #6175 ), #24193, .T. ) ;
#68126=VERTEX_POINT ( 'NONE', #15391 ) ;
#68163=LINE ( 'NONE', #35429, #1994 ) ;
#68164=CARTESIAN_POINT ( 'NONE',  ( 2.949999999999999734, 3.306546357697853240E-16, -2.699999999999999734 ) ) ;
#68200=ORIENTED_EDGE ( 'NONE', *, *, #4976, .T. ) ;
#68218=ORIENTED_EDGE ( 'NONE', *, *, #32730, .T. ) ;
#68219=CARTESIAN_POINT ( 'NONE',  ( 0.000000000000000000, 5.817072295949927426E-16, -4.750000000000000000 ) ) ;
#68234=VECTOR ( 'NONE', #3125, 1000.000000000000000 ) ;
#68295=VECTOR ( 'NONE', #5737, 999.9999999999998863 ) ;
#68486=FACE_OUTER_BOUND ( 'NONE', #63470, .T. ) ;
#68496=EDGE_CURVE ( 'NONE', #31992, #40854, #67137, .T. ) ;
#68583=CARTESIAN_POINT ( 'NONE',  ( 4.755015822784811164, -4.336808689942017736E-16, 0.000000000000000000 ) ) ;
#68608=DIRECTION ( 'NONE',  ( 0.000000000000000000, 0.000000000000000000, 1.000000000000000000 ) ) ;
#68676=CARTESIAN_POINT ( 'NONE',  ( 1.560000000000000053, 0.8660254037844389297, -1.500000000000000000 ) ) ;
#68805=ORIENTED_EDGE ( 'NONE', *, *, #19913, .T. ) ;
#68855=DIRECTION ( 'NONE',  ( -1.000000000000000000, 0.000000000000000000, 0.000000000000000000 ) ) ;
#68954=CARTESIAN_POINT ( 'NONE',  ( 2.426025403784448642, 0.000000000000000000, 2.168404344971008868E-16 ) ) ;
#69153=CARTESIAN_POINT ( 'NONE',  ( 2.750000000000000000, 3.306546357697853240E-16, -2.699999999999999734 ) ) ;
#69213=CARTESIAN_POINT ( 'NONE',  ( 1.560000000000000053, 1.732050807568878747, 7.017607234860990640E-28 ) ) ;
#69237=PLANE ( 'NONE',  #19245 ) ;
#69379=ORIENTED_EDGE ( 'NONE', *, *, #53507, .T. ) ;
#69491=AXIS2_PLACEMENT_3D ( 'NONE', #38433, #4613, #32773 ) ;
#69578=DIRECTION ( 'NONE',  ( -1.000000000000000000, -0.000000000000000000, -0.000000000000000000 ) ) ;
#69660=DIRECTION ( 'NONE',  ( 0.000000000000000000, 0.000000000000000000, 1.000000000000000000 ) ) ;
#69875=ORIENTED_EDGE ( 'NONE', *, *, #28494, .F. ) ;
#69932=CARTESIAN_POINT ( 'NONE',  ( 1.560000000000000053, -1.732050807568877859, -1.752539433813135784E-17 ) ) ;
#70048=DIRECTION ( 'NONE',  ( -1.000000000000000000, -0.000000000000000000, -0.000000000000000000 ) ) ;
#70104=VECTOR ( 'NONE', #11422, 1000.000000000000114 ) ;
#70414=VERTEX_POINT ( 'NONE', #39179 ) ;
#70761=CONICAL_SURFACE ( 'NONE', #5975, 2.055000000000000160, 0.7853981633974479459 ) ;
#70847=DIRECTION ( 'NONE',  ( -1.000000000000000000, -0.000000000000000000, -0.000000000000000000 ) ) ;
#70995=VERTEX_POINT ( 'NONE', #1866 ) ;
#71232=DIRECTION ( 'NONE',  ( 0.000000000000000000, 0.000000000000000000, 1.000000000000000000 ) ) ;
#71269=EDGE_LOOP ( 'NONE', ( #51012, #19630, #16846, #21630, #73890 ) ) ;
#71354=PLANE ( 'NONE',  #58763 ) ;
#71405=LINE ( 'NONE', #69932, #72022 ) ;
#71449=ORIENTED_EDGE ( 'NONE', *, *, #29498, .T. ) ;
#71455=CARTESIAN_POINT ( 'NONE',  ( 2.949999999999999734, 0.000000000000000000, 2.699999999999999734 ) ) ;
#71474=FACE_OUTER_BOUND ( 'NONE', #55306, .T. ) ;
#71553=VECTOR ( 'NONE', #14269, 1000.000000000000000 ) ;
#71605=UNCERTAINTY_MEASURE_WITH_UNIT (LENGTH_MEASURE( 1.000000000000000082E-05 ), #57337, 'distance_accuracy_value', 'NONE');
#71614=EDGE_CURVE ( 'NONE', #71835, #6105, #55180, .T. ) ;
#71702=ORIENTED_EDGE ( 'NONE', *, *, #63673, .T. ) ;
#71785=EDGE_CURVE ( 'NONE', #12127, #28934, #71405, .T. ) ;
#71835=VERTEX_POINT ( 'NONE', #47023 ) ;
#71844=LINE ( 'NONE', #36531, #27467 ) ;
#71872=CARTESIAN_POINT ( 'NONE',  ( 0.000000000000000000, 0.000000000000000000, 4.750000000000000000 ) ) ;
#72022=VECTOR ( 'NONE', #30084, 1000.000000000000114 ) ;
#72097=EDGE_CURVE ( 'NONE', #59464, #71835, #32416, .T. ) ;
#72274=CARTESIAN_POINT ( 'NONE',  ( 0.000000000000000000, 0.000000000000000000, 0.000000000000000000 ) ) ;
#72439=APPLICATION_CONTEXT ( 'automotive_design' ) ;
#72456=DIRECTION ( 'NONE',  ( -1.000000000000000000, -0.000000000000000000, -0.000000000000000000 ) ) ;
#72478=ORIENTED_EDGE ( 'NONE', *, *, #28494, .T. ) ;
#72582=DIRECTION ( 'NONE',  ( -1.000000000000000000, -0.000000000000000000, -0.000000000000000000 ) ) ;
#72658=VERTEX_POINT ( 'NONE', #50217 ) ;
#72750=DIRECTION ( 'NONE',  ( -0.000000000000000000, 0.5000000000000003331, -0.8660254037844384856 ) ) ;
#72775=VECTOR ( 'NONE', #15641, 1000.000000000000000 ) ;
#72779=FACE_OUTER_BOUND ( 'NONE', #57181, .T. ) ;
#72885=DIRECTION ( 'NONE',  ( -1.000000000000000000, -0.000000000000000000, -0.000000000000000000 ) ) ;
#72980=AXIS2_PLACEMENT_3D ( 'NONE', #54419, #66450, #48774 ) ;
#73088=EDGE_CURVE ( 'NONE', #43461, #26241, #34800, .T. ) ;
#73169=EDGE_CURVE ( 'NONE', #48451, #72658, #57285, .T. ) ;
#73218=AXIS2_PLACEMENT_3D ( 'NONE', #68164, #49744, #26454 ) ;
#73374=CARTESIAN_POINT ( 'NONE',  ( 1.560000000000000053, 0.8660254037844389297, 1.500000000000000000 ) ) ;
#73376=AXIS2_PLACEMENT_3D ( 'NONE', #7254, #51249, #57275 ) ;
#73503=LINE ( 'NONE', #27264, #17520 ) ;
#73754=DIRECTION ( 'NONE',  ( -1.000000000000000000, -0.000000000000000000, -0.000000000000000000 ) ) ;
#73890=ORIENTED_EDGE ( 'NONE', *, *, #15692, .F. ) ;
#74140=DIRECTION ( 'NONE',  ( -0.5000000000000042188, 1.060575238724903710E-16, -0.8660254037844361541 ) ) ;
#74183=AXIS2_PLACEMENT_3D ( 'NONE', #29533, #42323, #52473 ) ;
#74301=DIRECTION ( 'NONE',  ( -1.000000000000000000, 0.000000000000000000, 0.000000000000000000 ) ) ;
#74302=LINE ( 'NONE', #68676, #30056 ) ;
ENDSEC;
END-ISO-10303-21;
